ISO-10303-21;
HEADER;
/* Generated by software containing ST-Developer
 * from STEP Tools, Inc. (www.steptools.com) 
 */

FILE_DESCRIPTION(
/* description */ ('PAT-099'),
/* implementation_level */ '2;1');

FILE_NAME(
/* name */ 'Linear guide retaining cap (1).step',
/* time_stamp */ '2026-10-29T17:25:42-07:00',
/* author */ (''),
/* organization */ (''),
/* preprocessor_version */ 'ST-DEVELOPER v20.2',
/* originating_system */ 'Autodesk Translation Framework v15.17.0.0',
/* authorisation */ '');

FILE_SCHEMA (('AUTOMOTIVE_DESIGN { 1 0 10303 214 3 1 1 }'));
ENDSEC;

DATA;
#10=MECHANICAL_DESIGN_GEOMETRIC_PRESENTATION_REPRESENTATION('',(#340),#11035);
#290=SHAPE_REPRESENTATION_RELATIONSHIP('SRR','None',#11158,#315);
#315=ADVANCED_BREP_SHAPE_REPRESENTATION('',(#373),#11008);
#340=STYLED_ITEM('',(#11379),#373);
#373=MANIFOLD_SOLID_BREP('Body1',#4708);
#443=FACE_BOUND('',#1031,.T.);
#444=FACE_BOUND('',#1038,.T.);
#539=PLANE('',#5126);
#540=PLANE('',#5142);
#703=FACE_OUTER_BOUND('',#1026,.T.);
#704=FACE_OUTER_BOUND('',#1027,.T.);
#705=FACE_OUTER_BOUND('',#1028,.T.);
#706=FACE_OUTER_BOUND('',#1029,.T.);
#707=FACE_OUTER_BOUND('',#1030,.T.);
#708=FACE_OUTER_BOUND('',#1032,.T.);
#709=FACE_OUTER_BOUND('',#1033,.T.);
#710=FACE_OUTER_BOUND('',#1034,.T.);
#711=FACE_OUTER_BOUND('',#1035,.T.);
#712=FACE_OUTER_BOUND('',#1036,.T.);
#713=FACE_OUTER_BOUND('',#1037,.T.);
#1026=EDGE_LOOP('',(#3367,#3368,#3369,#3370));
#1027=EDGE_LOOP('',(#3371,#3372,#3373,#3374));
#1028=EDGE_LOOP('',(#3375,#3376,#3377,#3378));
#1029=EDGE_LOOP('',(#3379,#3380,#3381,#3382));
#1030=EDGE_LOOP('',(#3383,#3384,#3385,#3386,#3387,#3388,#3389,#3390));
#1031=EDGE_LOOP('',(#3391));
#1032=EDGE_LOOP('',(#3392,#3393,#3394,#3395));
#1033=EDGE_LOOP('',(#3396,#3397,#3398,#3399));
#1034=EDGE_LOOP('',(#3400,#3401,#3402,#3403));
#1035=EDGE_LOOP('',(#3404,#3405,#3406,#3407));
#1036=EDGE_LOOP('',(#3408,#3409,#3410,#3411));
#1037=EDGE_LOOP('',(#3412,#3413,#3414,#3415,#3416,#3417,#3418,#3419));
#1038=EDGE_LOOP('',(#3420));
#1395=LINE('',#7863,#1647);
#1396=LINE('',#7867,#1648);
#1397=LINE('',#7872,#1649);
#1398=LINE('',#7876,#1650);
#1399=LINE('',#7881,#1651);
#1400=LINE('',#7885,#1652);
#1401=LINE('',#7890,#1653);
#1402=LINE('',#7894,#1654);
#1403=LINE('',#7914,#1655);
#1647=VECTOR('',#5918,1.);
#1648=VECTOR('',#5921,1.);
#1649=VECTOR('',#5926,1.);
#1650=VECTOR('',#5929,1.);
#1651=VECTOR('',#5934,1.);
#1652=VECTOR('',#5937,1.);
#1653=VECTOR('',#5942,1.);
#1654=VECTOR('',#5945,1.);
#1655=VECTOR('',#5980,0.62);
#1895=CIRCLE('',#5115,0.225);
#1896=CIRCLE('',#5116,0.225);
#1897=CIRCLE('',#5118,0.225);
#1898=CIRCLE('',#5119,0.225);
#1899=CIRCLE('',#5121,0.225);
#1900=CIRCLE('',#5122,0.225);
#1901=CIRCLE('',#5124,0.225);
#1902=CIRCLE('',#5125,0.225);
#1903=CIRCLE('',#5127,1.9);
#1904=CIRCLE('',#5128,1.9);
#1905=CIRCLE('',#5129,1.9);
#1906=CIRCLE('',#5130,1.9);
#1907=CIRCLE('',#5131,0.62);
#1908=CIRCLE('',#5133,1.9);
#1909=CIRCLE('',#5135,1.9);
#1910=CIRCLE('',#5137,1.9);
#1911=CIRCLE('',#5139,1.9);
#1912=CIRCLE('',#5141,0.62);
#2220=VERTEX_POINT('',#7861);
#2221=VERTEX_POINT('',#7862);
#2222=VERTEX_POINT('',#7864);
#2223=VERTEX_POINT('',#7866);
#2224=VERTEX_POINT('',#7870);
#2225=VERTEX_POINT('',#7871);
#2226=VERTEX_POINT('',#7873);
#2227=VERTEX_POINT('',#7875);
#2228=VERTEX_POINT('',#7879);
#2229=VERTEX_POINT('',#7880);
#2230=VERTEX_POINT('',#7882);
#2231=VERTEX_POINT('',#7884);
#2232=VERTEX_POINT('',#7888);
#2233=VERTEX_POINT('',#7889);
#2234=VERTEX_POINT('',#7891);
#2235=VERTEX_POINT('',#7893);
#2236=VERTEX_POINT('',#7901);
#2237=VERTEX_POINT('',#7912);
#2660=EDGE_CURVE('',#2220,#2221,#1395,.T.);
#2661=EDGE_CURVE('',#2222,#2220,#1895,.T.);
#2662=EDGE_CURVE('',#2223,#2222,#1396,.T.);
#2663=EDGE_CURVE('',#2221,#2223,#1896,.T.);
#2664=EDGE_CURVE('',#2224,#2225,#1397,.T.);
#2665=EDGE_CURVE('',#2226,#2224,#1897,.T.);
#2666=EDGE_CURVE('',#2227,#2226,#1398,.T.);
#2667=EDGE_CURVE('',#2225,#2227,#1898,.T.);
#2668=EDGE_CURVE('',#2228,#2229,#1399,.T.);
#2669=EDGE_CURVE('',#2230,#2228,#1899,.T.);
#2670=EDGE_CURVE('',#2231,#2230,#1400,.T.);
#2671=EDGE_CURVE('',#2229,#2231,#1900,.T.);
#2672=EDGE_CURVE('',#2232,#2233,#1401,.T.);
#2673=EDGE_CURVE('',#2234,#2232,#1901,.T.);
#2674=EDGE_CURVE('',#2235,#2234,#1402,.T.);
#2675=EDGE_CURVE('',#2233,#2235,#1902,.T.);
#2676=EDGE_CURVE('',#2230,#2220,#1903,.T.);
#2677=EDGE_CURVE('',#2226,#2228,#1904,.T.);
#2678=EDGE_CURVE('',#2234,#2224,#1905,.T.);
#2679=EDGE_CURVE('',#2222,#2232,#1906,.T.);
#2680=EDGE_CURVE('',#2236,#2236,#1907,.T.);
#2681=EDGE_CURVE('',#2235,#2225,#1908,.T.);
#2682=EDGE_CURVE('',#2227,#2229,#1909,.T.);
#2683=EDGE_CURVE('',#2231,#2221,#1910,.T.);
#2684=EDGE_CURVE('',#2223,#2233,#1911,.T.);
#2685=EDGE_CURVE('',#2237,#2237,#1912,.T.);
#2686=EDGE_CURVE('',#2237,#2236,#1403,.T.);
#3367=ORIENTED_EDGE('',*,*,#2660,.F.);
#3368=ORIENTED_EDGE('',*,*,#2661,.F.);
#3369=ORIENTED_EDGE('',*,*,#2662,.F.);
#3370=ORIENTED_EDGE('',*,*,#2663,.F.);
#3371=ORIENTED_EDGE('',*,*,#2664,.F.);
#3372=ORIENTED_EDGE('',*,*,#2665,.F.);
#3373=ORIENTED_EDGE('',*,*,#2666,.F.);
#3374=ORIENTED_EDGE('',*,*,#2667,.F.);
#3375=ORIENTED_EDGE('',*,*,#2668,.F.);
#3376=ORIENTED_EDGE('',*,*,#2669,.F.);
#3377=ORIENTED_EDGE('',*,*,#2670,.F.);
#3378=ORIENTED_EDGE('',*,*,#2671,.F.);
#3379=ORIENTED_EDGE('',*,*,#2672,.F.);
#3380=ORIENTED_EDGE('',*,*,#2673,.F.);
#3381=ORIENTED_EDGE('',*,*,#2674,.F.);
#3382=ORIENTED_EDGE('',*,*,#2675,.F.);
#3383=ORIENTED_EDGE('',*,*,#2661,.T.);
#3384=ORIENTED_EDGE('',*,*,#2676,.F.);
#3385=ORIENTED_EDGE('',*,*,#2669,.T.);
#3386=ORIENTED_EDGE('',*,*,#2677,.F.);
#3387=ORIENTED_EDGE('',*,*,#2665,.T.);
#3388=ORIENTED_EDGE('',*,*,#2678,.F.);
#3389=ORIENTED_EDGE('',*,*,#2673,.T.);
#3390=ORIENTED_EDGE('',*,*,#2679,.F.);
#3391=ORIENTED_EDGE('',*,*,#2680,.F.);
#3392=ORIENTED_EDGE('',*,*,#2664,.T.);
#3393=ORIENTED_EDGE('',*,*,#2681,.F.);
#3394=ORIENTED_EDGE('',*,*,#2674,.T.);
#3395=ORIENTED_EDGE('',*,*,#2678,.T.);
#3396=ORIENTED_EDGE('',*,*,#2666,.T.);
#3397=ORIENTED_EDGE('',*,*,#2677,.T.);
#3398=ORIENTED_EDGE('',*,*,#2668,.T.);
#3399=ORIENTED_EDGE('',*,*,#2682,.F.);
#3400=ORIENTED_EDGE('',*,*,#2660,.T.);
#3401=ORIENTED_EDGE('',*,*,#2683,.F.);
#3402=ORIENTED_EDGE('',*,*,#2670,.T.);
#3403=ORIENTED_EDGE('',*,*,#2676,.T.);
#3404=ORIENTED_EDGE('',*,*,#2662,.T.);
#3405=ORIENTED_EDGE('',*,*,#2679,.T.);
#3406=ORIENTED_EDGE('',*,*,#2672,.T.);
#3407=ORIENTED_EDGE('',*,*,#2684,.F.);
#3408=ORIENTED_EDGE('',*,*,#2685,.F.);
#3409=ORIENTED_EDGE('',*,*,#2686,.T.);
#3410=ORIENTED_EDGE('',*,*,#2680,.T.);
#3411=ORIENTED_EDGE('',*,*,#2686,.F.);
#3412=ORIENTED_EDGE('',*,*,#2663,.T.);
#3413=ORIENTED_EDGE('',*,*,#2684,.T.);
#3414=ORIENTED_EDGE('',*,*,#2675,.T.);
#3415=ORIENTED_EDGE('',*,*,#2681,.T.);
#3416=ORIENTED_EDGE('',*,*,#2667,.T.);
#3417=ORIENTED_EDGE('',*,*,#2682,.T.);
#3418=ORIENTED_EDGE('',*,*,#2671,.T.);
#3419=ORIENTED_EDGE('',*,*,#2683,.T.);
#3420=ORIENTED_EDGE('',*,*,#2685,.T.);
#4337=CYLINDRICAL_SURFACE('',#5114,0.225);
#4338=CYLINDRICAL_SURFACE('',#5117,0.225);
#4339=CYLINDRICAL_SURFACE('',#5120,0.225);
#4340=CYLINDRICAL_SURFACE('',#5123,0.225);
#4341=CYLINDRICAL_SURFACE('',#5132,1.9);
#4342=CYLINDRICAL_SURFACE('',#5134,1.9);
#4343=CYLINDRICAL_SURFACE('',#5136,1.9);
#4344=CYLINDRICAL_SURFACE('',#5138,1.9);
#4345=CYLINDRICAL_SURFACE('',#5140,0.62);
#4468=ADVANCED_FACE('',(#703),#4337,.F.);
#4469=ADVANCED_FACE('',(#704),#4338,.F.);
#4470=ADVANCED_FACE('',(#705),#4339,.F.);
#4471=ADVANCED_FACE('',(#706),#4340,.F.);
#4472=ADVANCED_FACE('',(#707,#443),#539,.F.);
#4473=ADVANCED_FACE('',(#708),#4341,.T.);
#4474=ADVANCED_FACE('',(#709),#4342,.T.);
#4475=ADVANCED_FACE('',(#710),#4343,.T.);
#4476=ADVANCED_FACE('',(#711),#4344,.T.);
#4477=ADVANCED_FACE('',(#712),#4345,.F.);
#4478=ADVANCED_FACE('',(#713,#444),#540,.T.);
#4708=CLOSED_SHELL('',(#4468,#4469,#4470,#4471,#4472,#4473,#4474,#4475,
#4476,#4477,#4478));
#5113=AXIS2_PLACEMENT_3D('',#7859,#5914,#5915);
#5114=AXIS2_PLACEMENT_3D('',#7860,#5916,#5917);
#5115=AXIS2_PLACEMENT_3D('',#7865,#5919,#5920);
#5116=AXIS2_PLACEMENT_3D('',#7868,#5922,#5923);
#5117=AXIS2_PLACEMENT_3D('',#7869,#5924,#5925);
#5118=AXIS2_PLACEMENT_3D('',#7874,#5927,#5928);
#5119=AXIS2_PLACEMENT_3D('',#7877,#5930,#5931);
#5120=AXIS2_PLACEMENT_3D('',#7878,#5932,#5933);
#5121=AXIS2_PLACEMENT_3D('',#7883,#5935,#5936);
#5122=AXIS2_PLACEMENT_3D('',#7886,#5938,#5939);
#5123=AXIS2_PLACEMENT_3D('',#7887,#5940,#5941);
#5124=AXIS2_PLACEMENT_3D('',#7892,#5943,#5944);
#5125=AXIS2_PLACEMENT_3D('',#7895,#5946,#5947);
#5126=AXIS2_PLACEMENT_3D('',#7896,#5948,#5949);
#5127=AXIS2_PLACEMENT_3D('',#7897,#5950,#5951);
#5128=AXIS2_PLACEMENT_3D('',#7898,#5952,#5953);
#5129=AXIS2_PLACEMENT_3D('',#7899,#5954,#5955);
#5130=AXIS2_PLACEMENT_3D('',#7900,#5956,#5957);
#5131=AXIS2_PLACEMENT_3D('',#7902,#5958,#5959);
#5132=AXIS2_PLACEMENT_3D('',#7903,#5960,#5961);
#5133=AXIS2_PLACEMENT_3D('',#7904,#5962,#5963);
#5134=AXIS2_PLACEMENT_3D('',#7905,#5964,#5965);
#5135=AXIS2_PLACEMENT_3D('',#7906,#5966,#5967);
#5136=AXIS2_PLACEMENT_3D('',#7907,#5968,#5969);
#5137=AXIS2_PLACEMENT_3D('',#7908,#5970,#5971);
#5138=AXIS2_PLACEMENT_3D('',#7909,#5972,#5973);
#5139=AXIS2_PLACEMENT_3D('',#7910,#5974,#5975);
#5140=AXIS2_PLACEMENT_3D('',#7911,#5976,#5977);
#5141=AXIS2_PLACEMENT_3D('',#7913,#5978,#5979);
#5142=AXIS2_PLACEMENT_3D('',#7915,#5981,#5982);
#5914=DIRECTION('axis',(0.,0.,1.));
#5915=DIRECTION('refdir',(1.,0.,0.));
#5916=DIRECTION('center_axis',(1.,0.,0.));
#5917=DIRECTION('ref_axis',(0.,-0.707106781186549,0.707106781186546));
#5918=DIRECTION('',(1.,0.,0.));
#5919=DIRECTION('center_axis',(1.,0.,0.));
#5920=DIRECTION('ref_axis',(0.,0.,-1.));
#5921=DIRECTION('',(-1.,0.,0.));
#5922=DIRECTION('center_axis',(-1.,0.,0.));
#5923=DIRECTION('ref_axis',(0.,0.,-1.));
#5924=DIRECTION('center_axis',(1.,0.,0.));
#5925=DIRECTION('ref_axis',(0.,0.707106781186548,-0.707106781186547));
#5926=DIRECTION('',(1.,0.,0.));
#5927=DIRECTION('center_axis',(1.,0.,0.));
#5928=DIRECTION('ref_axis',(0.,0.,-1.));
#5929=DIRECTION('',(-1.,0.,0.));
#5930=DIRECTION('center_axis',(-1.,0.,0.));
#5931=DIRECTION('ref_axis',(0.,0.,-1.));
#5932=DIRECTION('center_axis',(1.,0.,0.));
#5933=DIRECTION('ref_axis',(0.,0.707106781186549,0.707106781186546));
#5934=DIRECTION('',(1.,0.,0.));
#5935=DIRECTION('center_axis',(1.,0.,0.));
#5936=DIRECTION('ref_axis',(0.,0.,-1.));
#5937=DIRECTION('',(-1.,0.,0.));
#5938=DIRECTION('center_axis',(-1.,0.,0.));
#5939=DIRECTION('ref_axis',(0.,0.,-1.));
#5940=DIRECTION('center_axis',(1.,0.,0.));
#5941=DIRECTION('ref_axis',(0.,-0.707106781186547,-0.707106781186548));
#5942=DIRECTION('',(1.,0.,0.));
#5943=DIRECTION('center_axis',(1.,0.,0.));
#5944=DIRECTION('ref_axis',(0.,0.,-1.));
#5945=DIRECTION('',(-1.,0.,0.));
#5946=DIRECTION('center_axis',(-1.,0.,0.));
#5947=DIRECTION('ref_axis',(0.,0.,-1.));
#5948=DIRECTION('center_axis',(1.,0.,0.));
#5949=DIRECTION('ref_axis',(0.,0.,-1.));
#5950=DIRECTION('center_axis',(1.,0.,0.));
#5951=DIRECTION('ref_axis',(0.,0.,-1.));
#5952=DIRECTION('center_axis',(1.,0.,0.));
#5953=DIRECTION('ref_axis',(0.,0.,-1.));
#5954=DIRECTION('center_axis',(1.,0.,0.));
#5955=DIRECTION('ref_axis',(0.,0.,-1.));
#5956=DIRECTION('center_axis',(1.,0.,0.));
#5957=DIRECTION('ref_axis',(0.,0.,-1.));
#5958=DIRECTION('center_axis',(-1.,0.,0.));
#5959=DIRECTION('ref_axis',(0.,0.,-1.));
#5960=DIRECTION('center_axis',(1.,0.,0.));
#5961=DIRECTION('ref_axis',(0.,-1.22464679914735E-16,1.));
#5962=DIRECTION('center_axis',(1.,0.,0.));
#5963=DIRECTION('ref_axis',(0.,0.,-1.));
#5964=DIRECTION('center_axis',(1.,0.,0.));
#5965=DIRECTION('ref_axis',(0.,0.,-1.));
#5966=DIRECTION('center_axis',(1.,0.,0.));
#5967=DIRECTION('ref_axis',(0.,0.,-1.));
#5968=DIRECTION('center_axis',(1.,0.,0.));
#5969=DIRECTION('ref_axis',(0.,0.,-1.));
#5970=DIRECTION('center_axis',(1.,0.,0.));
#5971=DIRECTION('ref_axis',(0.,0.,-1.));
#5972=DIRECTION('center_axis',(1.,0.,0.));
#5973=DIRECTION('ref_axis',(0.,0.,-1.));
#5974=DIRECTION('center_axis',(1.,0.,0.));
#5975=DIRECTION('ref_axis',(0.,0.,-1.));
#5976=DIRECTION('center_axis',(1.,0.,0.));
#5977=DIRECTION('ref_axis',(0.,0.,-1.));
#5978=DIRECTION('center_axis',(-1.,0.,0.));
#5979=DIRECTION('ref_axis',(0.,0.,-1.));
#5980=DIRECTION('',(-1.,0.,0.));
#5981=DIRECTION('center_axis',(1.,0.,0.));
#5982=DIRECTION('ref_axis',(0.,0.,-1.));
#7859=CARTESIAN_POINT('',(0.,0.,0.));
#7860=CARTESIAN_POINT('Origin',(12.9,1.2,4.05));
#7861=CARTESIAN_POINT('',(13.,1.26887332488551,3.83580040821884));
#7862=CARTESIAN_POINT('',(13.3,1.26887332488551,3.83580040821884));
#7863=CARTESIAN_POINT('',(12.9,1.26887332488551,3.83580040821884));
#7864=CARTESIAN_POINT('',(13.,1.41419959178116,3.98112667511449));
#7865=CARTESIAN_POINT('Origin',(13.,1.2,4.05));
#7866=CARTESIAN_POINT('',(13.3,1.41419959178116,3.98112667511449));
#7867=CARTESIAN_POINT('',(12.9,1.41419959178116,3.98112667511449));
#7868=CARTESIAN_POINT('Origin',(13.3,1.2,4.05));
#7869=CARTESIAN_POINT('Origin',(12.9,-1.2,6.45));
#7870=CARTESIAN_POINT('',(13.,-1.26887332488551,6.66419959178116));
#7871=CARTESIAN_POINT('',(13.3,-1.26887332488551,6.66419959178116));
#7872=CARTESIAN_POINT('',(12.9,-1.26887332488551,6.66419959178116));
#7873=CARTESIAN_POINT('',(13.,-1.41419959178116,6.51887332488551));
#7874=CARTESIAN_POINT('Origin',(13.,-1.2,6.45));
#7875=CARTESIAN_POINT('',(13.3,-1.41419959178116,6.51887332488551));
#7876=CARTESIAN_POINT('',(12.9,-1.41419959178116,6.51887332488551));
#7877=CARTESIAN_POINT('Origin',(13.3,-1.2,6.45));
#7878=CARTESIAN_POINT('Origin',(12.9,-1.2,4.05));
#7879=CARTESIAN_POINT('',(13.,-1.41419959178116,3.98112667511449));
#7880=CARTESIAN_POINT('',(13.3,-1.41419959178116,3.98112667511449));
#7881=CARTESIAN_POINT('',(12.9,-1.41419959178116,3.98112667511449));
#7882=CARTESIAN_POINT('',(13.,-1.26887332488551,3.83580040821884));
#7883=CARTESIAN_POINT('Origin',(13.,-1.2,4.05));
#7884=CARTESIAN_POINT('',(13.3,-1.26887332488551,3.83580040821884));
#7885=CARTESIAN_POINT('',(12.9,-1.26887332488551,3.83580040821884));
#7886=CARTESIAN_POINT('Origin',(13.3,-1.2,4.05));
#7887=CARTESIAN_POINT('Origin',(12.9,1.2,6.45));
#7888=CARTESIAN_POINT('',(13.,1.41419959178116,6.51887332488551));
#7889=CARTESIAN_POINT('',(13.3,1.41419959178116,6.51887332488551));
#7890=CARTESIAN_POINT('',(12.9,1.41419959178116,6.51887332488551));
#7891=CARTESIAN_POINT('',(13.,1.26887332488551,6.66419959178116));
#7892=CARTESIAN_POINT('Origin',(13.,1.2,6.45));
#7893=CARTESIAN_POINT('',(13.3,1.26887332488551,6.66419959178116));
#7894=CARTESIAN_POINT('',(12.9,1.26887332488551,6.66419959178116));
#7895=CARTESIAN_POINT('Origin',(13.3,1.2,6.45));
#7896=CARTESIAN_POINT('Origin',(13.,0.,5.25));
#7897=CARTESIAN_POINT('Origin',(13.,0.,5.25));
#7898=CARTESIAN_POINT('Origin',(13.,0.,5.25));
#7899=CARTESIAN_POINT('Origin',(13.,0.,5.25));
#7900=CARTESIAN_POINT('Origin',(13.,0.,5.25));
#7901=CARTESIAN_POINT('',(13.,-7.59281015471359E-17,5.87));
#7902=CARTESIAN_POINT('Origin',(13.,0.,5.25));
#7903=CARTESIAN_POINT('Origin',(13.,0.,5.25));
#7904=CARTESIAN_POINT('Origin',(13.3,0.,5.25));
#7905=CARTESIAN_POINT('Origin',(13.,0.,5.25));
#7906=CARTESIAN_POINT('Origin',(13.3,0.,5.25));
#7907=CARTESIAN_POINT('Origin',(13.,0.,5.25));
#7908=CARTESIAN_POINT('Origin',(13.3,0.,5.25));
#7909=CARTESIAN_POINT('Origin',(13.,0.,5.25));
#7910=CARTESIAN_POINT('Origin',(13.3,0.,5.25));
#7911=CARTESIAN_POINT('Origin',(13.,0.,5.25));
#7912=CARTESIAN_POINT('',(13.3,-7.59281015471359E-17,5.87));
#7913=CARTESIAN_POINT('Origin',(13.3,0.,5.25));
#7914=CARTESIAN_POINT('',(13.,-7.59281015471359E-17,5.87));
#7915=CARTESIAN_POINT('Origin',(13.3,0.,5.25));
#10975=UNCERTAINTY_MEASURE_WITH_UNIT(LENGTH_MEASURE(0.001),#11036,
'DISTANCE_ACCURACY_VALUE',
'Maximum model space distance between geometric entities at asserted c
onnectivities');
#11002=UNCERTAINTY_MEASURE_WITH_UNIT(LENGTH_MEASURE(0.001),#11036,
'DISTANCE_ACCURACY_VALUE',
'Maximum model space distance between geometric entities at asserted c
onnectivities');
#11008=(
GEOMETRIC_REPRESENTATION_CONTEXT(3)
GLOBAL_UNCERTAINTY_ASSIGNED_CONTEXT((#10975))
GLOBAL_UNIT_ASSIGNED_CONTEXT((#11036,#11038,#11039))
REPRESENTATION_CONTEXT('','3D')
);
#11035=(
GEOMETRIC_REPRESENTATION_CONTEXT(3)
GLOBAL_UNCERTAINTY_ASSIGNED_CONTEXT((#11002))
GLOBAL_UNIT_ASSIGNED_CONTEXT((#11036,#11038,#11039))
REPRESENTATION_CONTEXT('','3D')
);
#11036=(
LENGTH_UNIT()
NAMED_UNIT(*)
SI_UNIT(.CENTI.,.METRE.)
);
#11038=(
NAMED_UNIT(*)
PLANE_ANGLE_UNIT()
SI_UNIT($,.RADIAN.)
);
#11039=(
NAMED_UNIT(*)
SI_UNIT($,.STERADIAN.)
SOLID_ANGLE_UNIT()
);
#11045=SHAPE_DEFINITION_REPRESENTATION(#11077,#11158);
#11077=PRODUCT_DEFINITION_SHAPE('',$,#11191);
#11158=SHAPE_REPRESENTATION('',(#5113),#11008);
#11185=PRODUCT_DEFINITION_CONTEXT('part definition',#11283,'design');
#11191=PRODUCT_DEFINITION('Linear guide retaining cap (1)',
'Linear guide retaining cap (1)',#11223,#11185);
#11223=PRODUCT_DEFINITION_FORMATION('',$,#11290);
#11283=APPLICATION_CONTEXT(
'Core Data for Automotive Mechanical Design Process');
#11284=PRODUCT_CONTEXT('part definition',#11283,'mechanical');
#11290=PRODUCT('Linear guide retaining cap (1)',
'Linear guide retaining cap (1)','Linear guide retaining cap (1)',(#11284));
#11373=COLOUR_RGB('Sky Blue',0.24,0.69,0.87);
#11374=FILL_AREA_STYLE_COLOUR('',#11373);
#11375=FILL_AREA_STYLE('',(#11374));
#11376=SURFACE_STYLE_FILL_AREA(#11375);
#11377=SURFACE_SIDE_STYLE('',(#11376));
#11378=SURFACE_STYLE_USAGE(.BOTH.,#11377);
#11379=PRESENTATION_STYLE_ASSIGNMENT((#11378));
ENDSEC;
END-ISO-10303-21;
